ISO-10303-21;
HEADER;
/* Generated by software containing ST-Developer
 * from STEP Tools, Inc. (www.steptools.com) 
 */

FILE_DESCRIPTION(
/* description */ ('Horizontal push-pull toggle clamp'),
/* implementation_level */ '2;1');

FILE_NAME(
/* name */ 'Hex Nut - M8.step',
/* time_stamp */ '2026-10-27T21:21:09-07:00',
/* author */ (''),
/* organization */ (''),
/* preprocessor_version */ 'ST-DEVELOPER v20.2',
/* originating_system */ 'Autodesk Translation Framework v15.17.0.0',
/* authorisation */ '');

FILE_SCHEMA (('AUTOMOTIVE_DESIGN { 1 0 10303 214 3 1 1 }'));
ENDSEC;

DATA;
#10=MECHANICAL_DESIGN_GEOMETRIC_PRESENTATION_REPRESENTATION('',(#192),#4791);
#24=(
BOUNDED_CURVE()
B_SPLINE_CURVE(2,(#4436,#4437,#4438),.UNSPECIFIED.,.F.,.F.)
B_SPLINE_CURVE_WITH_KNOTS((3,3),(0.14973948338295,0.97160236658079),
 .UNSPECIFIED.)
CURVE()
GEOMETRIC_REPRESENTATION_ITEM()
RATIONAL_B_SPLINE_CURVE((1.07140024848292,1.23714644374248,1.07140024848292))
REPRESENTATION_ITEM('')
);
#25=(
BOUNDED_CURVE()
B_SPLINE_CURVE(2,(#4440,#4441,#4442),.UNSPECIFIED.,.F.,.F.)
B_SPLINE_CURVE_WITH_KNOTS((3,3),(0.14973948338295,0.971602366580789),
 .UNSPECIFIED.)
CURVE()
GEOMETRIC_REPRESENTATION_ITEM()
RATIONAL_B_SPLINE_CURVE((1.07140024848292,1.23714644374248,1.07140024848292))
REPRESENTATION_ITEM('')
);
#26=(
BOUNDED_CURVE()
B_SPLINE_CURVE(2,(#4447,#4448,#4449),.UNSPECIFIED.,.F.,.F.)
B_SPLINE_CURVE_WITH_KNOTS((3,3),(0.14973948338295,0.97160236658079),
 .UNSPECIFIED.)
CURVE()
GEOMETRIC_REPRESENTATION_ITEM()
RATIONAL_B_SPLINE_CURVE((1.07140024848292,1.23714644374248,1.07140024848292))
REPRESENTATION_ITEM('')
);
#27=(
BOUNDED_CURVE()
B_SPLINE_CURVE(2,(#4451,#4452,#4453),.UNSPECIFIED.,.F.,.F.)
B_SPLINE_CURVE_WITH_KNOTS((3,3),(0.14973948338295,0.97160236658079),
 .UNSPECIFIED.)
CURVE()
GEOMETRIC_REPRESENTATION_ITEM()
RATIONAL_B_SPLINE_CURVE((1.07140024848292,1.23714644374248,1.07140024848292))
REPRESENTATION_ITEM('')
);
#28=(
BOUNDED_CURVE()
B_SPLINE_CURVE(2,(#4455,#4456,#4457),.UNSPECIFIED.,.F.,.F.)
B_SPLINE_CURVE_WITH_KNOTS((3,3),(0.14973948338295,0.971602366580789),
 .UNSPECIFIED.)
CURVE()
GEOMETRIC_REPRESENTATION_ITEM()
RATIONAL_B_SPLINE_CURVE((1.07140024848292,1.23714644374248,1.07140024848292))
REPRESENTATION_ITEM('')
);
#29=(
BOUNDED_CURVE()
B_SPLINE_CURVE(2,(#4458,#4459,#4460),.UNSPECIFIED.,.F.,.F.)
B_SPLINE_CURVE_WITH_KNOTS((3,3),(0.14973948338295,0.97160236658079),
 .UNSPECIFIED.)
CURVE()
GEOMETRIC_REPRESENTATION_ITEM()
RATIONAL_B_SPLINE_CURVE((1.07140024848292,1.23714644374248,1.07140024848292))
REPRESENTATION_ITEM('')
);
#30=(
BOUNDED_CURVE()
B_SPLINE_CURVE(2,(#4467,#4468,#4469),.UNSPECIFIED.,.F.,.F.)
B_SPLINE_CURVE_WITH_KNOTS((3,3),(0.14973948338295,0.97160236658079),
 .UNSPECIFIED.)
CURVE()
GEOMETRIC_REPRESENTATION_ITEM()
RATIONAL_B_SPLINE_CURVE((1.07140024848292,1.23714644374248,1.07140024848292))
REPRESENTATION_ITEM('')
);
#31=(
BOUNDED_CURVE()
B_SPLINE_CURVE(2,(#4471,#4472,#4473),.UNSPECIFIED.,.F.,.F.)
B_SPLINE_CURVE_WITH_KNOTS((3,3),(0.14973948338295,0.97160236658079),
 .UNSPECIFIED.)
CURVE()
GEOMETRIC_REPRESENTATION_ITEM()
RATIONAL_B_SPLINE_CURVE((1.07140024848292,1.23714644374248,1.07140024848292))
REPRESENTATION_ITEM('')
);
#32=(
BOUNDED_CURVE()
B_SPLINE_CURVE(2,(#4475,#4476,#4477),.UNSPECIFIED.,.F.,.F.)
B_SPLINE_CURVE_WITH_KNOTS((3,3),(0.14973948338295,0.971602366580789),
 .UNSPECIFIED.)
CURVE()
GEOMETRIC_REPRESENTATION_ITEM()
RATIONAL_B_SPLINE_CURVE((1.07140024848292,1.23714644374248,1.07140024848292))
REPRESENTATION_ITEM('')
);
#33=(
BOUNDED_CURVE()
B_SPLINE_CURVE(2,(#4479,#4480,#4481),.UNSPECIFIED.,.F.,.F.)
B_SPLINE_CURVE_WITH_KNOTS((3,3),(0.14973948338295,0.97160236658079),
 .UNSPECIFIED.)
CURVE()
GEOMETRIC_REPRESENTATION_ITEM()
RATIONAL_B_SPLINE_CURVE((1.07140024848292,1.23714644374248,1.07140024848292))
REPRESENTATION_ITEM('')
);
#34=(
BOUNDED_CURVE()
B_SPLINE_CURVE(2,(#4483,#4484,#4485),.UNSPECIFIED.,.F.,.F.)
B_SPLINE_CURVE_WITH_KNOTS((3,3),(0.14973948338295,0.97160236658079),
 .UNSPECIFIED.)
CURVE()
GEOMETRIC_REPRESENTATION_ITEM()
RATIONAL_B_SPLINE_CURVE((1.07140024848292,1.23714644374248,1.07140024848292))
REPRESENTATION_ITEM('')
);
#35=(
BOUNDED_CURVE()
B_SPLINE_CURVE(2,(#4486,#4487,#4488),.UNSPECIFIED.,.F.,.F.)
B_SPLINE_CURVE_WITH_KNOTS((3,3),(0.14973948338295,0.971602366580789),
 .UNSPECIFIED.)
CURVE()
GEOMETRIC_REPRESENTATION_ITEM()
RATIONAL_B_SPLINE_CURVE((1.07140024848292,1.23714644374248,1.07140024848292))
REPRESENTATION_ITEM('')
);
#153=CONICAL_SURFACE('',#2978,0.734027674973257,1.0471975511966);
#154=CONICAL_SURFACE('',#2980,0.734027674973257,1.0471975511966);
#166=SHAPE_REPRESENTATION_RELATIONSHIP('SRR','None',#4872,#179);
#179=ADVANCED_BREP_SHAPE_REPRESENTATION('',(#204),#4785);
#192=STYLED_ITEM('',(#5030),#204);
#204=MANIFOLD_SOLID_BREP('Body1',#2637);
#247=FACE_BOUND('',#676,.T.);
#248=FACE_BOUND('',#678,.T.);
#342=PLANE('',#2982);
#343=PLANE('',#2983);
#344=PLANE('',#2984);
#345=PLANE('',#2988);
#346=PLANE('',#2989);
#347=PLANE('',#2990);
#348=PLANE('',#2991);
#349=PLANE('',#2992);
#478=FACE_OUTER_BOUND('',#666,.T.);
#479=FACE_OUTER_BOUND('',#667,.T.);
#480=FACE_OUTER_BOUND('',#668,.T.);
#481=FACE_OUTER_BOUND('',#669,.T.);
#482=FACE_OUTER_BOUND('',#670,.T.);
#483=FACE_OUTER_BOUND('',#671,.T.);
#484=FACE_OUTER_BOUND('',#672,.T.);
#485=FACE_OUTER_BOUND('',#673,.T.);
#486=FACE_OUTER_BOUND('',#674,.T.);
#487=FACE_OUTER_BOUND('',#675,.T.);
#488=FACE_OUTER_BOUND('',#677,.T.);
#666=EDGE_LOOP('',(#2307,#2308,#2309,#2310,#2311,#2312,#2313,#2314,#2315));
#667=EDGE_LOOP('',(#2316,#2317,#2318,#2319,#2320,#2321,#2322,#2323,#2324));
#668=EDGE_LOOP('',(#2325,#2326,#2327,#2328));
#669=EDGE_LOOP('',(#2329,#2330,#2331,#2332));
#670=EDGE_LOOP('',(#2333,#2334,#2335,#2336));
#671=EDGE_LOOP('',(#2337,#2338,#2339,#2340));
#672=EDGE_LOOP('',(#2341,#2342,#2343,#2344));
#673=EDGE_LOOP('',(#2345,#2346,#2347,#2348));
#674=EDGE_LOOP('',(#2349,#2350,#2351,#2352));
#675=EDGE_LOOP('',(#2353));
#676=EDGE_LOOP('',(#2354));
#677=EDGE_LOOP('',(#2355));
#678=EDGE_LOOP('',(#2356));
#771=CIRCLE('',#2979,0.6175);
#772=CIRCLE('',#2981,0.6175);
#773=CIRCLE('',#2986,0.338975);
#774=CIRCLE('',#2987,0.338975);
#991=LINE('',#4444,#1211);
#992=LINE('',#4465,#1212);
#993=LINE('',#4490,#1213);
#994=LINE('',#4491,#1214);
#995=LINE('',#4493,#1215);
#996=LINE('',#4495,#1216);
#997=LINE('',#4500,#1217);
#998=LINE('',#4503,#1218);
#999=LINE('',#4505,#1219);
#1211=VECTOR('',#3649,0.734027674973257);
#1212=VECTOR('',#3656,0.734027674973257);
#1213=VECTOR('',#3659,1.);
#1214=VECTOR('',#3660,1.);
#1215=VECTOR('',#3663,1.);
#1216=VECTOR('',#3666,1.);
#1217=VECTOR('',#3671,0.4);
#1218=VECTOR('',#3676,1.);
#1219=VECTOR('',#3679,1.);
#1409=VERTEX_POINT('',#4434);
#1410=VERTEX_POINT('',#4435);
#1411=VERTEX_POINT('',#4439);
#1412=VERTEX_POINT('',#4443);
#1413=VERTEX_POINT('',#4446);
#1414=VERTEX_POINT('',#4450);
#1415=VERTEX_POINT('',#4454);
#1416=VERTEX_POINT('',#4462);
#1417=VERTEX_POINT('',#4464);
#1418=VERTEX_POINT('',#4466);
#1419=VERTEX_POINT('',#4470);
#1420=VERTEX_POINT('',#4474);
#1421=VERTEX_POINT('',#4478);
#1422=VERTEX_POINT('',#4482);
#1423=VERTEX_POINT('',#4497);
#1424=VERTEX_POINT('',#4499);
#1715=EDGE_CURVE('',#1409,#1410,#24,.T.);
#1716=EDGE_CURVE('',#1411,#1409,#25,.T.);
#1717=EDGE_CURVE('',#1411,#1412,#991,.T.);
#1718=EDGE_CURVE('',#1412,#1412,#771,.T.);
#1719=EDGE_CURVE('',#1413,#1411,#26,.T.);
#1720=EDGE_CURVE('',#1414,#1413,#27,.T.);
#1721=EDGE_CURVE('',#1415,#1414,#28,.T.);
#1722=EDGE_CURVE('',#1410,#1415,#29,.T.);
#1723=EDGE_CURVE('',#1416,#1416,#772,.T.);
#1724=EDGE_CURVE('',#1416,#1417,#992,.T.);
#1725=EDGE_CURVE('',#1418,#1417,#30,.T.);
#1726=EDGE_CURVE('',#1419,#1418,#31,.T.);
#1727=EDGE_CURVE('',#1420,#1419,#32,.T.);
#1728=EDGE_CURVE('',#1421,#1420,#33,.T.);
#1729=EDGE_CURVE('',#1422,#1421,#34,.T.);
#1730=EDGE_CURVE('',#1417,#1422,#35,.T.);
#1731=EDGE_CURVE('',#1413,#1422,#993,.T.);
#1732=EDGE_CURVE('',#1414,#1421,#994,.T.);
#1733=EDGE_CURVE('',#1411,#1417,#995,.T.);
#1734=EDGE_CURVE('',#1409,#1418,#996,.T.);
#1735=EDGE_CURVE('',#1423,#1423,#773,.F.);
#1736=EDGE_CURVE('',#1423,#1424,#997,.T.);
#1737=EDGE_CURVE('',#1424,#1424,#774,.F.);
#1738=EDGE_CURVE('',#1410,#1419,#998,.T.);
#1739=EDGE_CURVE('',#1415,#1420,#999,.T.);
#2307=ORIENTED_EDGE('',*,*,#1715,.F.);
#2308=ORIENTED_EDGE('',*,*,#1716,.F.);
#2309=ORIENTED_EDGE('',*,*,#1717,.T.);
#2310=ORIENTED_EDGE('',*,*,#1718,.F.);
#2311=ORIENTED_EDGE('',*,*,#1717,.F.);
#2312=ORIENTED_EDGE('',*,*,#1719,.F.);
#2313=ORIENTED_EDGE('',*,*,#1720,.F.);
#2314=ORIENTED_EDGE('',*,*,#1721,.F.);
#2315=ORIENTED_EDGE('',*,*,#1722,.F.);
#2316=ORIENTED_EDGE('',*,*,#1723,.F.);
#2317=ORIENTED_EDGE('',*,*,#1724,.T.);
#2318=ORIENTED_EDGE('',*,*,#1725,.F.);
#2319=ORIENTED_EDGE('',*,*,#1726,.F.);
#2320=ORIENTED_EDGE('',*,*,#1727,.F.);
#2321=ORIENTED_EDGE('',*,*,#1728,.F.);
#2322=ORIENTED_EDGE('',*,*,#1729,.F.);
#2323=ORIENTED_EDGE('',*,*,#1730,.F.);
#2324=ORIENTED_EDGE('',*,*,#1724,.F.);
#2325=ORIENTED_EDGE('',*,*,#1720,.T.);
#2326=ORIENTED_EDGE('',*,*,#1731,.T.);
#2327=ORIENTED_EDGE('',*,*,#1729,.T.);
#2328=ORIENTED_EDGE('',*,*,#1732,.F.);
#2329=ORIENTED_EDGE('',*,*,#1719,.T.);
#2330=ORIENTED_EDGE('',*,*,#1733,.T.);
#2331=ORIENTED_EDGE('',*,*,#1730,.T.);
#2332=ORIENTED_EDGE('',*,*,#1731,.F.);
#2333=ORIENTED_EDGE('',*,*,#1716,.T.);
#2334=ORIENTED_EDGE('',*,*,#1734,.T.);
#2335=ORIENTED_EDGE('',*,*,#1725,.T.);
#2336=ORIENTED_EDGE('',*,*,#1733,.F.);
#2337=ORIENTED_EDGE('',*,*,#1735,.F.);
#2338=ORIENTED_EDGE('',*,*,#1736,.T.);
#2339=ORIENTED_EDGE('',*,*,#1737,.T.);
#2340=ORIENTED_EDGE('',*,*,#1736,.F.);
#2341=ORIENTED_EDGE('',*,*,#1715,.T.);
#2342=ORIENTED_EDGE('',*,*,#1738,.T.);
#2343=ORIENTED_EDGE('',*,*,#1726,.T.);
#2344=ORIENTED_EDGE('',*,*,#1734,.F.);
#2345=ORIENTED_EDGE('',*,*,#1721,.T.);
#2346=ORIENTED_EDGE('',*,*,#1732,.T.);
#2347=ORIENTED_EDGE('',*,*,#1728,.T.);
#2348=ORIENTED_EDGE('',*,*,#1739,.F.);
#2349=ORIENTED_EDGE('',*,*,#1722,.T.);
#2350=ORIENTED_EDGE('',*,*,#1739,.T.);
#2351=ORIENTED_EDGE('',*,*,#1727,.T.);
#2352=ORIENTED_EDGE('',*,*,#1738,.F.);
#2353=ORIENTED_EDGE('',*,*,#1723,.T.);
#2354=ORIENTED_EDGE('',*,*,#1735,.T.);
#2355=ORIENTED_EDGE('',*,*,#1718,.T.);
#2356=ORIENTED_EDGE('',*,*,#1737,.F.);
#2468=CYLINDRICAL_SURFACE('',#2985,0.338975);
#2594=ADVANCED_FACE('',(#478),#153,.T.);
#2595=ADVANCED_FACE('',(#479),#154,.T.);
#2596=ADVANCED_FACE('',(#480),#342,.T.);
#2597=ADVANCED_FACE('',(#481),#343,.T.);
#2598=ADVANCED_FACE('',(#482),#344,.T.);
#2599=ADVANCED_FACE('',(#483),#2468,.F.);
#2600=ADVANCED_FACE('',(#484),#345,.T.);
#2601=ADVANCED_FACE('',(#485),#346,.T.);
#2602=ADVANCED_FACE('',(#486),#347,.T.);
#2603=ADVANCED_FACE('',(#487,#247),#348,.T.);
#2604=ADVANCED_FACE('',(#488,#248),#349,.F.);
#2637=CLOSED_SHELL('',(#2594,#2595,#2596,#2597,#2598,#2599,#2600,#2601,
#2602,#2603,#2604));
#2977=AXIS2_PLACEMENT_3D('',#4432,#3645,#3646);
#2978=AXIS2_PLACEMENT_3D('',#4433,#3647,#3648);
#2979=AXIS2_PLACEMENT_3D('',#4445,#3650,#3651);
#2980=AXIS2_PLACEMENT_3D('',#4461,#3652,#3653);
#2981=AXIS2_PLACEMENT_3D('',#4463,#3654,#3655);
#2982=AXIS2_PLACEMENT_3D('',#4489,#3657,#3658);
#2983=AXIS2_PLACEMENT_3D('',#4492,#3661,#3662);
#2984=AXIS2_PLACEMENT_3D('',#4494,#3664,#3665);
#2985=AXIS2_PLACEMENT_3D('',#4496,#3667,#3668);
#2986=AXIS2_PLACEMENT_3D('',#4498,#3669,#3670);
#2987=AXIS2_PLACEMENT_3D('',#4501,#3672,#3673);
#2988=AXIS2_PLACEMENT_3D('',#4502,#3674,#3675);
#2989=AXIS2_PLACEMENT_3D('',#4504,#3677,#3678);
#2990=AXIS2_PLACEMENT_3D('',#4506,#3680,#3681);
#2991=AXIS2_PLACEMENT_3D('',#4507,#3682,#3683);
#2992=AXIS2_PLACEMENT_3D('',#4508,#3684,#3685);
#3645=DIRECTION('axis',(0.,0.,1.));
#3646=DIRECTION('refdir',(1.,0.,0.));
#3647=DIRECTION('center_axis',(0.,1.,0.));
#3648=DIRECTION('ref_axis',(1.,0.,0.));
#3649=DIRECTION('',(0.866025403784439,-0.5,1.06057523872491E-16));
#3650=DIRECTION('center_axis',(0.,-1.,0.));
#3651=DIRECTION('ref_axis',(1.,0.,0.));
#3652=DIRECTION('center_axis',(0.,-1.,0.));
#3653=DIRECTION('ref_axis',(1.,0.,0.));
#3654=DIRECTION('center_axis',(0.,1.,0.));
#3655=DIRECTION('ref_axis',(1.,0.,0.));
#3656=DIRECTION('',(-0.866025403784439,-0.5,-1.06057523872491E-16));
#3657=DIRECTION('center_axis',(1.4792020664489E-16,0.,-1.));
#3658=DIRECTION('ref_axis',(-1.,0.,-1.4792020664489E-16));
#3659=DIRECTION('',(0.,1.,0.));
#3660=DIRECTION('',(0.,1.,0.));
#3661=DIRECTION('center_axis',(-0.866025403784439,0.,-0.5));
#3662=DIRECTION('ref_axis',(-0.5,0.,0.866025403784439));
#3663=DIRECTION('',(0.,1.,0.));
#3664=DIRECTION('center_axis',(-0.866025403784439,0.,0.5));
#3665=DIRECTION('ref_axis',(0.5,0.,0.866025403784439));
#3666=DIRECTION('',(0.,1.,0.));
#3667=DIRECTION('center_axis',(0.,1.,0.));
#3668=DIRECTION('ref_axis',(1.,0.,0.));
#3669=DIRECTION('center_axis',(0.,1.,0.));
#3670=DIRECTION('ref_axis',(1.,0.,0.));
#3671=DIRECTION('',(0.,-1.,0.));
#3672=DIRECTION('center_axis',(0.,1.,0.));
#3673=DIRECTION('ref_axis',(1.,0.,0.));
#3674=DIRECTION('center_axis',(-2.95840413289779E-16,0.,1.));
#3675=DIRECTION('ref_axis',(1.,0.,2.95840413289779E-16));
#3676=DIRECTION('',(0.,1.,0.));
#3677=DIRECTION('center_axis',(0.866025403784439,0.,-0.5));
#3678=DIRECTION('ref_axis',(-0.5,0.,-0.866025403784439));
#3679=DIRECTION('',(0.,1.,0.));
#3680=DIRECTION('center_axis',(0.866025403784439,0.,0.5));
#3681=DIRECTION('ref_axis',(0.5,0.,-0.866025403784439));
#3682=DIRECTION('center_axis',(0.,1.,0.));
#3683=DIRECTION('ref_axis',(1.,0.,0.));
#3684=DIRECTION('center_axis',(0.,1.,0.));
#3685=DIRECTION('ref_axis',(1.,0.,0.));
#4432=CARTESIAN_POINT('',(0.,0.,0.));
#4433=CARTESIAN_POINT('Origin',(0.,0.067277284513851,0.));
#4434=CARTESIAN_POINT('',(-0.375277674973257,0.0768195421087395,0.65));
#4435=CARTESIAN_POINT('',(0.375277674973257,0.0768195421087395,0.65));
#4436=CARTESIAN_POINT('Ctrl Pts',(-0.375277674973257,0.0768195421087395,
0.65));
#4437=CARTESIAN_POINT('Ctrl Pts',(1.66533453693773E-13,-0.0315137912242439,
0.65));
#4438=CARTESIAN_POINT('Ctrl Pts',(0.375277674973257,0.0768195421087394,
0.65));
#4439=CARTESIAN_POINT('',(-0.750555349946514,0.0768195421087394,-9.19165206894919E-17));
#4440=CARTESIAN_POINT('Ctrl Pts',(-0.750555349946514,0.0768195421087394,
-9.19165206894919E-17));
#4441=CARTESIAN_POINT('Ctrl Pts',(-0.562916512459802,-0.0315137912242434,
0.325000000000144));
#4442=CARTESIAN_POINT('Ctrl Pts',(-0.375277674973257,0.0768195421087395,
0.65));
#4443=CARTESIAN_POINT('',(-0.6175,-2.77555756156289E-17,-7.5621939847349E-17));
#4444=CARTESIAN_POINT('',(-0.734027674973257,0.067277284513851,-8.98924642641573E-17));
#4445=CARTESIAN_POINT('Origin',(0.,0.,0.));
#4446=CARTESIAN_POINT('',(-0.375277674973257,0.0768195421087395,-0.65));
#4447=CARTESIAN_POINT('Ctrl Pts',(-0.375277674973257,0.0768195421087395,
-0.65));
#4448=CARTESIAN_POINT('Ctrl Pts',(-0.562916512459968,-0.0315137912242437,
-0.324999999999856));
#4449=CARTESIAN_POINT('Ctrl Pts',(-0.750555349946514,0.0768195421087395,
-9.19165206894919E-17));
#4450=CARTESIAN_POINT('',(0.375277674973257,0.0768195421087395,-0.65));
#4451=CARTESIAN_POINT('Ctrl Pts',(0.375277674973257,0.0768195421087395,
-0.65));
#4452=CARTESIAN_POINT('Ctrl Pts',(-1.66144875635155E-13,-0.0315137912242437,
-0.65));
#4453=CARTESIAN_POINT('Ctrl Pts',(-0.375277674973257,0.0768195421087395,
-0.65));
#4454=CARTESIAN_POINT('',(0.750555349946514,0.0768195421087394,0.));
#4455=CARTESIAN_POINT('Ctrl Pts',(0.750555349946514,0.0768195421087394,
0.));
#4456=CARTESIAN_POINT('Ctrl Pts',(0.562916512459802,-0.0315137912242436,
-0.325000000000144));
#4457=CARTESIAN_POINT('Ctrl Pts',(0.375277674973257,0.0768195421087395,
-0.65));
#4458=CARTESIAN_POINT('Ctrl Pts',(0.375277674973257,0.0768195421087394,
0.65));
#4459=CARTESIAN_POINT('Ctrl Pts',(0.562916512459968,-0.0315137912242439,
0.324999999999856));
#4460=CARTESIAN_POINT('Ctrl Pts',(0.750555349946514,0.0768195421087394,
0.));
#4461=CARTESIAN_POINT('Origin',(0.,0.612722715486149,0.));
#4462=CARTESIAN_POINT('',(-0.6175,0.68,-7.5621939847349E-17));
#4463=CARTESIAN_POINT('Origin',(0.,0.68,0.));
#4464=CARTESIAN_POINT('',(-0.750555349946514,0.603180457891261,-9.19165206894919E-17));
#4465=CARTESIAN_POINT('',(-0.734027674973257,0.612722715486149,-8.98924642641573E-17));
#4466=CARTESIAN_POINT('',(-0.375277674973257,0.603180457891261,0.65));
#4467=CARTESIAN_POINT('Ctrl Pts',(-0.375277674973257,0.603180457891261,
0.65));
#4468=CARTESIAN_POINT('Ctrl Pts',(-0.562916512459968,0.711513791224243,
0.324999999999856));
#4469=CARTESIAN_POINT('Ctrl Pts',(-0.750555349946514,0.603180457891261,
-9.19165206894919E-17));
#4470=CARTESIAN_POINT('',(0.375277674973257,0.603180457891261,0.65));
#4471=CARTESIAN_POINT('Ctrl Pts',(0.375277674973257,0.603180457891261,0.65));
#4472=CARTESIAN_POINT('Ctrl Pts',(-1.66755498298699E-13,0.711513791224244,
0.65));
#4473=CARTESIAN_POINT('Ctrl Pts',(-0.375277674973257,0.603180457891261,
0.65));
#4474=CARTESIAN_POINT('',(0.750555349946514,0.603180457891261,0.));
#4475=CARTESIAN_POINT('Ctrl Pts',(0.750555349946514,0.603180457891261,0.));
#4476=CARTESIAN_POINT('Ctrl Pts',(0.562916512459802,0.711513791224244,0.325000000000144));
#4477=CARTESIAN_POINT('Ctrl Pts',(0.375277674973257,0.603180457891261,0.65));
#4478=CARTESIAN_POINT('',(0.375277674973257,0.603180457891261,-0.65));
#4479=CARTESIAN_POINT('Ctrl Pts',(0.375277674973257,0.603180457891261,-0.65));
#4480=CARTESIAN_POINT('Ctrl Pts',(0.562916512459969,0.711513791224244,-0.324999999999856));
#4481=CARTESIAN_POINT('Ctrl Pts',(0.750555349946514,0.603180457891261,0.));
#4482=CARTESIAN_POINT('',(-0.375277674973257,0.603180457891261,-0.65));
#4483=CARTESIAN_POINT('Ctrl Pts',(-0.375277674973257,0.603180457891261,
-0.65));
#4484=CARTESIAN_POINT('Ctrl Pts',(1.66422431391311E-13,0.711513791224244,
-0.65));
#4485=CARTESIAN_POINT('Ctrl Pts',(0.375277674973257,0.603180457891261,-0.65));
#4486=CARTESIAN_POINT('Ctrl Pts',(-0.750555349946514,0.603180457891261,
-9.19165206894919E-17));
#4487=CARTESIAN_POINT('Ctrl Pts',(-0.562916512459802,0.711513791224244,
-0.325000000000144));
#4488=CARTESIAN_POINT('Ctrl Pts',(-0.375277674973257,0.603180457891261,
-0.65));
#4489=CARTESIAN_POINT('Origin',(0.375277674973257,0.,-0.65));
#4490=CARTESIAN_POINT('',(-0.375277674973257,0.,-0.65));
#4491=CARTESIAN_POINT('',(0.375277674973257,0.,-0.65));
#4492=CARTESIAN_POINT('Origin',(-0.375277674973257,0.,-0.65));
#4493=CARTESIAN_POINT('',(-0.750555349946514,0.,-9.19165206894919E-17));
#4494=CARTESIAN_POINT('Origin',(-0.750555349946514,0.,-9.19165206894919E-17));
#4495=CARTESIAN_POINT('',(-0.375277674973257,0.,0.65));
#4496=CARTESIAN_POINT('Origin',(0.,0.,0.));
#4497=CARTESIAN_POINT('',(-0.338975,0.68,4.15124648740974E-17));
#4498=CARTESIAN_POINT('Origin',(0.,0.68,0.));
#4499=CARTESIAN_POINT('',(-0.338975,0.,4.15124648740974E-17));
#4500=CARTESIAN_POINT('',(-0.338975,0.,4.15124648740974E-17));
#4501=CARTESIAN_POINT('Origin',(0.,0.,0.));
#4502=CARTESIAN_POINT('Origin',(-0.375277674973257,0.,0.65));
#4503=CARTESIAN_POINT('',(0.375277674973257,0.,0.65));
#4504=CARTESIAN_POINT('Origin',(0.750555349946514,0.,0.));
#4505=CARTESIAN_POINT('',(0.750555349946514,0.,0.));
#4506=CARTESIAN_POINT('Origin',(0.375277674973257,0.,0.65));
#4507=CARTESIAN_POINT('Origin',(0.,0.68,-1.11022302462516E-16));
#4508=CARTESIAN_POINT('Origin',(0.,0.,-1.11022302462516E-16));
#4766=UNCERTAINTY_MEASURE_WITH_UNIT(LENGTH_MEASURE(0.001),#4792,
'DISTANCE_ACCURACY_VALUE',
'Maximum model space distance between geometric entities at asserted c
onnectivities');
#4772=UNCERTAINTY_MEASURE_WITH_UNIT(LENGTH_MEASURE(0.001),#4792,
'DISTANCE_ACCURACY_VALUE',
'Maximum model space distance between geometric entities at asserted c
onnectivities');
#4785=(
GEOMETRIC_REPRESENTATION_CONTEXT(3)
GLOBAL_UNCERTAINTY_ASSIGNED_CONTEXT((#4766))
GLOBAL_UNIT_ASSIGNED_CONTEXT((#4792,#4794,#4795))
REPRESENTATION_CONTEXT('','3D')
);
#4791=(
GEOMETRIC_REPRESENTATION_CONTEXT(3)
GLOBAL_UNCERTAINTY_ASSIGNED_CONTEXT((#4772))
GLOBAL_UNIT_ASSIGNED_CONTEXT((#4792,#4794,#4795))
REPRESENTATION_CONTEXT('','3D')
);
#4792=(
LENGTH_UNIT()
NAMED_UNIT(*)
SI_UNIT(.CENTI.,.METRE.)
);
#4794=(
NAMED_UNIT(*)
PLANE_ANGLE_UNIT()
SI_UNIT($,.RADIAN.)
);
#4795=(
NAMED_UNIT(*)
SI_UNIT($,.STERADIAN.)
SOLID_ANGLE_UNIT()
);
#4808=SHAPE_DEFINITION_REPRESENTATION(#4827,#4872);
#4827=PRODUCT_DEFINITION_SHAPE('',$,#4891);
#4872=SHAPE_REPRESENTATION('',(#2977),#4785);
#4878=PRODUCT_DEFINITION_CONTEXT('part definition',#4934,'design');
#4891=PRODUCT_DEFINITION('Hex Nut - M8','Hex Nut - M8',#4909,#4878);
#4909=PRODUCT_DEFINITION_FORMATION('',$,#4948);
#4934=APPLICATION_CONTEXT(
'Core Data for Automotive Mechanical Design Process');
#4935=PRODUCT_CONTEXT('part definition',#4934,'mechanical');
#4948=PRODUCT('Hex Nut - M8','Hex Nut - M8','Hex Nut - M8',(#4935));
#5024=COLOUR_RGB('Black',0.12,0.14,0.17);
#5025=FILL_AREA_STYLE_COLOUR('',#5024);
#5026=FILL_AREA_STYLE('',(#5025));
#5027=SURFACE_STYLE_FILL_AREA(#5026);
#5028=SURFACE_SIDE_STYLE('',(#5027));
#5029=SURFACE_STYLE_USAGE(.BOTH.,#5028);
#5030=PRESENTATION_STYLE_ASSIGNMENT((#5029));
ENDSEC;
END-ISO-10303-21;
